ISO-10303-21;
HEADER;
/* Generated by software containing ST-Developer
 * from STEP Tools, Inc. (www.steptools.com) 
 */

FILE_DESCRIPTION(
/* description */ ('Four-bar parallelogram arm'),
/* implementation_level */ '2;1');

FILE_NAME(
/* name */ 'Rear inner spacer (2).step',
/* time_stamp */ '2026-10-28T03:24:55-07:00',
/* author */ (''),
/* organization */ (''),
/* preprocessor_version */ 'ST-DEVELOPER v20.2',
/* originating_system */ 'Autodesk Translation Framework v15.17.0.0',
/* authorisation */ '');

FILE_SCHEMA (('AUTOMOTIVE_DESIGN { 1 0 10303 214 3 1 1 }'));
ENDSEC;

DATA;
#10=MECHANICAL_DESIGN_GEOMETRIC_PRESENTATION_REPRESENTATION('',(#671),#14512);
#563=SHAPE_REPRESENTATION_RELATIONSHIP('SRR','None',#14788,#613);
#613=ADVANCED_BREP_SHAPE_REPRESENTATION('',(#727),#14503);
#671=STYLED_ITEM('',(#15080),#727);
#727=MANIFOLD_SOLID_BREP('Body1',#7377);
#982=FACE_BOUND('',#2234,.T.);
#983=FACE_BOUND('',#2236,.T.);
#1171=PLANE('',#8809);
#1172=PLANE('',#8810);
#1564=FACE_OUTER_BOUND('',#2231,.T.);
#1565=FACE_OUTER_BOUND('',#2232,.T.);
#1566=FACE_OUTER_BOUND('',#2233,.T.);
#1567=FACE_OUTER_BOUND('',#2235,.T.);
#2231=EDGE_LOOP('',(#6524,#6525,#6526,#6527));
#2232=EDGE_LOOP('',(#6528,#6529,#6530,#6531));
#2233=EDGE_LOOP('',(#6532));
#2234=EDGE_LOOP('',(#6533));
#2235=EDGE_LOOP('',(#6534));
#2236=EDGE_LOOP('',(#6535));
#2661=LINE('',#14129,#3055);
#2662=LINE('',#14135,#3056);
#3055=VECTOR('',#11053,0.504999999999999);
#3056=VECTOR('',#11060,0.699999999999999);
#3495=CIRCLE('',#8804,0.504999999999999);
#3496=CIRCLE('',#8805,0.504999999999999);
#3497=CIRCLE('',#8807,0.699999999999999);
#3498=CIRCLE('',#8808,0.699999999999999);
#4063=VERTEX_POINT('',#14126);
#4064=VERTEX_POINT('',#14128);
#4065=VERTEX_POINT('',#14132);
#4066=VERTEX_POINT('',#14134);
#4893=EDGE_CURVE('',#4063,#4063,#3495,.T.);
#4894=EDGE_CURVE('',#4063,#4064,#2661,.T.);
#4895=EDGE_CURVE('',#4064,#4064,#3496,.T.);
#4896=EDGE_CURVE('',#4065,#4065,#3497,.T.);
#4897=EDGE_CURVE('',#4065,#4066,#2662,.T.);
#4898=EDGE_CURVE('',#4066,#4066,#3498,.T.);
#6524=ORIENTED_EDGE('',*,*,#4893,.F.);
#6525=ORIENTED_EDGE('',*,*,#4894,.T.);
#6526=ORIENTED_EDGE('',*,*,#4895,.T.);
#6527=ORIENTED_EDGE('',*,*,#4894,.F.);
#6528=ORIENTED_EDGE('',*,*,#4896,.F.);
#6529=ORIENTED_EDGE('',*,*,#4897,.T.);
#6530=ORIENTED_EDGE('',*,*,#4898,.T.);
#6531=ORIENTED_EDGE('',*,*,#4897,.F.);
#6532=ORIENTED_EDGE('',*,*,#4896,.T.);
#6533=ORIENTED_EDGE('',*,*,#4893,.T.);
#6534=ORIENTED_EDGE('',*,*,#4898,.F.);
#6535=ORIENTED_EDGE('',*,*,#4895,.F.);
#6883=CYLINDRICAL_SURFACE('',#8803,0.504999999999999);
#6884=CYLINDRICAL_SURFACE('',#8806,0.699999999999999);
#7269=ADVANCED_FACE('',(#1564),#6883,.F.);
#7270=ADVANCED_FACE('',(#1565),#6884,.T.);
#7271=ADVANCED_FACE('',(#1566,#982),#1171,.T.);
#7272=ADVANCED_FACE('',(#1567,#983),#1172,.F.);
#7377=CLOSED_SHELL('',(#7269,#7270,#7271,#7272));
#8802=AXIS2_PLACEMENT_3D('',#14124,#11047,#11048);
#8803=AXIS2_PLACEMENT_3D('',#14125,#11049,#11050);
#8804=AXIS2_PLACEMENT_3D('',#14127,#11051,#11052);
#8805=AXIS2_PLACEMENT_3D('',#14130,#11054,#11055);
#8806=AXIS2_PLACEMENT_3D('',#14131,#11056,#11057);
#8807=AXIS2_PLACEMENT_3D('',#14133,#11058,#11059);
#8808=AXIS2_PLACEMENT_3D('',#14136,#11061,#11062);
#8809=AXIS2_PLACEMENT_3D('',#14137,#11063,#11064);
#8810=AXIS2_PLACEMENT_3D('',#14138,#11065,#11066);
#11047=DIRECTION('axis',(0.,0.,1.));
#11048=DIRECTION('refdir',(1.,0.,0.));
#11049=DIRECTION('center_axis',(0.,1.,0.));
#11050=DIRECTION('ref_axis',(1.,0.,0.));
#11051=DIRECTION('center_axis',(0.,-1.,0.));
#11052=DIRECTION('ref_axis',(1.,0.,0.));
#11053=DIRECTION('',(0.,-1.,0.));
#11054=DIRECTION('center_axis',(0.,-1.,0.));
#11055=DIRECTION('ref_axis',(1.,0.,0.));
#11056=DIRECTION('center_axis',(0.,1.,0.));
#11057=DIRECTION('ref_axis',(1.,0.,0.));
#11058=DIRECTION('center_axis',(0.,1.,0.));
#11059=DIRECTION('ref_axis',(1.,0.,0.));
#11060=DIRECTION('',(0.,-1.,0.));
#11061=DIRECTION('center_axis',(0.,1.,0.));
#11062=DIRECTION('ref_axis',(1.,0.,0.));
#11063=DIRECTION('center_axis',(0.,1.,0.));
#11064=DIRECTION('ref_axis',(1.,0.,0.));
#11065=DIRECTION('center_axis',(0.,1.,0.));
#11066=DIRECTION('ref_axis',(1.,0.,0.));
#14124=CARTESIAN_POINT('',(0.,0.,0.));
#14125=CARTESIAN_POINT('Origin',(20.,1.05,8.));
#14126=CARTESIAN_POINT('',(19.495,2.5,8.));
#14127=CARTESIAN_POINT('Origin',(20.,2.5,8.));
#14128=CARTESIAN_POINT('',(19.495,1.05,8.));
#14129=CARTESIAN_POINT('',(19.495,1.05,8.));
#14130=CARTESIAN_POINT('Origin',(20.,1.05,8.));
#14131=CARTESIAN_POINT('Origin',(20.,1.05,8.));
#14132=CARTESIAN_POINT('',(19.3,2.5,8.));
#14133=CARTESIAN_POINT('Origin',(20.,2.5,8.));
#14134=CARTESIAN_POINT('',(19.3,1.05,8.));
#14135=CARTESIAN_POINT('',(19.3,1.05,8.));
#14136=CARTESIAN_POINT('Origin',(20.,1.05,8.));
#14137=CARTESIAN_POINT('Origin',(20.,2.5,8.));
#14138=CARTESIAN_POINT('Origin',(20.,1.05,8.));
#14446=UNCERTAINTY_MEASURE_WITH_UNIT(LENGTH_MEASURE(0.001),#14513,
'DISTANCE_ACCURACY_VALUE',
'Maximum model space distance between geometric entities at asserted c
onnectivities');
#14455=UNCERTAINTY_MEASURE_WITH_UNIT(LENGTH_MEASURE(0.001),#14513,
'DISTANCE_ACCURACY_VALUE',
'Maximum model space distance between geometric entities at asserted c
onnectivities');
#14503=(
GEOMETRIC_REPRESENTATION_CONTEXT(3)
GLOBAL_UNCERTAINTY_ASSIGNED_CONTEXT((#14446))
GLOBAL_UNIT_ASSIGNED_CONTEXT((#14513,#14515,#14516))
REPRESENTATION_CONTEXT('','3D')
);
#14512=(
GEOMETRIC_REPRESENTATION_CONTEXT(3)
GLOBAL_UNCERTAINTY_ASSIGNED_CONTEXT((#14455))
GLOBAL_UNIT_ASSIGNED_CONTEXT((#14513,#14515,#14516))
REPRESENTATION_CONTEXT('','3D')
);
#14513=(
LENGTH_UNIT()
NAMED_UNIT(*)
SI_UNIT(.CENTI.,.METRE.)
);
#14515=(
NAMED_UNIT(*)
PLANE_ANGLE_UNIT()
SI_UNIT($,.RADIAN.)
);
#14516=(
NAMED_UNIT(*)
SI_UNIT($,.STERADIAN.)
SOLID_ANGLE_UNIT()
);
#14564=SHAPE_DEFINITION_REPRESENTATION(#14680,#14788);
#14680=PRODUCT_DEFINITION_SHAPE('',$,#14845);
#14788=SHAPE_REPRESENTATION('',(#8802),#14503);
#14797=PRODUCT_DEFINITION_CONTEXT('part definition',#14967,'design');
#14845=PRODUCT_DEFINITION('Rear inner spacer (2)','Rear inner spacer (2)',
#14901,#14797);
#14901=PRODUCT_DEFINITION_FORMATION('',$,#15016);
#14967=APPLICATION_CONTEXT(
'Core Data for Automotive Mechanical Design Process');
#14968=PRODUCT_CONTEXT('part definition',#14967,'mechanical');
#15016=PRODUCT('Rear inner spacer (2)','Rear inner spacer (2)',
'Rear inner spacer (2)',(#14968));
#15074=COLOUR_RGB('Sky Blue',0.24,0.69,0.87);
#15075=FILL_AREA_STYLE_COLOUR('',#15074);
#15076=FILL_AREA_STYLE('',(#15075));
#15077=SURFACE_STYLE_FILL_AREA(#15076);
#15078=SURFACE_SIDE_STYLE('',(#15077));
#15079=SURFACE_STYLE_USAGE(.BOTH.,#15078);
#15080=PRESENTATION_STYLE_ASSIGNMENT((#15079));
ENDSEC;
END-ISO-10303-21;
